ISO-10303-21;
HEADER;
/* Generated by software containing ST-Developer
 * from STEP Tools, Inc. (www.steptools.com) 
 */

FILE_DESCRIPTION(
/* description */ ('Quick-return (Whitworth) mechanism'),
/* implementation_level */ '2;1');

FILE_NAME(
/* name */ 'M5x14 Cap Screw.step',
/* time_stamp */ '2026-10-28T03:25:57-07:00',
/* author */ (''),
/* organization */ (''),
/* preprocessor_version */ 'ST-DEVELOPER v20.2',
/* originating_system */ 'Autodesk Translation Framework v15.17.0.0',
/* authorisation */ '');

FILE_SCHEMA (('AUTOMOTIVE_DESIGN { 1 0 10303 214 3 1 1 }'));
ENDSEC;

DATA;
#10=MECHANICAL_DESIGN_GEOMETRIC_PRESENTATION_REPRESENTATION('',(#540),#14878);
#12=ORIENTED_CLOSED_SHELL('',*,#7895,.F.);
#15=BREP_WITH_VOIDS('Body1',#7896,(#12));
#358=CONICAL_SURFACE('',#9295,0.4,0.785398163397448);
#359=CONICAL_SURFACE('',#9299,0.41,0.785398163397448);
#360=CONICAL_SURFACE('',#9303,0.26,0.463647609000806);
#444=SHAPE_REPRESENTATION_RELATIONSHIP('SRR','None',#15119,#488);
#488=ADVANCED_BREP_SHAPE_REPRESENTATION('',(#15),#14876);
#540=STYLED_ITEM('',(#15413),#15);
#780=FACE_BOUND('',#2150,.T.);
#1025=PLANE('',#9283);
#1026=PLANE('',#9284);
#1027=PLANE('',#9285);
#1028=PLANE('',#9286);
#1029=PLANE('',#9287);
#1030=PLANE('',#9288);
#1031=PLANE('',#9289);
#1032=PLANE('',#9290);
#1033=PLANE('',#9291);
#1034=PLANE('',#9293);
#1035=PLANE('',#9301);
#1481=FACE_OUTER_BOUND('',#2136,.T.);
#1482=FACE_OUTER_BOUND('',#2137,.T.);
#1483=FACE_OUTER_BOUND('',#2138,.T.);
#1484=FACE_OUTER_BOUND('',#2139,.T.);
#1485=FACE_OUTER_BOUND('',#2140,.T.);
#1486=FACE_OUTER_BOUND('',#2141,.T.);
#1487=FACE_OUTER_BOUND('',#2142,.T.);
#1488=FACE_OUTER_BOUND('',#2143,.T.);
#1489=FACE_OUTER_BOUND('',#2144,.T.);
#1490=FACE_OUTER_BOUND('',#2145,.T.);
#1491=FACE_OUTER_BOUND('',#2146,.T.);
#1492=FACE_OUTER_BOUND('',#2147,.T.);
#1493=FACE_OUTER_BOUND('',#2148,.T.);
#1494=FACE_OUTER_BOUND('',#2149,.T.);
#1495=FACE_OUTER_BOUND('',#2151,.T.);
#1496=FACE_OUTER_BOUND('',#2152,.T.);
#2136=EDGE_LOOP('',(#7090,#7091,#7092,#7093));
#2137=EDGE_LOOP('',(#7094,#7095,#7096,#7097));
#2138=EDGE_LOOP('',(#7098,#7099,#7100,#7101));
#2139=EDGE_LOOP('',(#7102,#7103,#7104,#7105));
#2140=EDGE_LOOP('',(#7106,#7107,#7108,#7109));
#2141=EDGE_LOOP('',(#7110,#7111,#7112,#7113));
#2142=EDGE_LOOP('',(#7114,#7115,#7116,#7117,#7118,#7119));
#2143=EDGE_LOOP('',(#7120,#7121,#7122,#7123,#7124,#7125));
#2144=EDGE_LOOP('',(#7126));
#2145=EDGE_LOOP('',(#7127));
#2146=EDGE_LOOP('',(#7128,#7129,#7130,#7131));
#2147=EDGE_LOOP('',(#7132,#7133,#7134,#7135));
#2148=EDGE_LOOP('',(#7136,#7137,#7138,#7139));
#2149=EDGE_LOOP('',(#7140));
#2150=EDGE_LOOP('',(#7141));
#2151=EDGE_LOOP('',(#7142,#7143,#7144,#7145));
#2152=EDGE_LOOP('',(#7146,#7147,#7148,#7149));
#2647=LINE('',#14576,#3170);
#2648=LINE('',#14578,#3171);
#2649=LINE('',#14580,#3172);
#2650=LINE('',#14581,#3173);
#2651=LINE('',#14584,#3174);
#2652=LINE('',#14586,#3175);
#2653=LINE('',#14587,#3176);
#2654=LINE('',#14590,#3177);
#2655=LINE('',#14592,#3178);
#2656=LINE('',#14593,#3179);
#2657=LINE('',#14596,#3180);
#2658=LINE('',#14598,#3181);
#2659=LINE('',#14599,#3182);
#2660=LINE('',#14602,#3183);
#2661=LINE('',#14604,#3184);
#2662=LINE('',#14605,#3185);
#2663=LINE('',#14607,#3186);
#2664=LINE('',#14608,#3187);
#2665=LINE('',#14620,#3188);
#2666=LINE('',#14624,#3189);
#2667=LINE('',#14628,#3190);
#2668=LINE('',#14635,#3191);
#2669=LINE('',#14637,#3192);
#3170=VECTOR('',#11674,1.);
#3171=VECTOR('',#11675,1.);
#3172=VECTOR('',#11676,1.);
#3173=VECTOR('',#11677,1.);
#3174=VECTOR('',#11680,1.);
#3175=VECTOR('',#11681,1.);
#3176=VECTOR('',#11682,1.);
#3177=VECTOR('',#11685,1.);
#3178=VECTOR('',#11686,1.);
#3179=VECTOR('',#11687,1.);
#3180=VECTOR('',#11690,1.);
#3181=VECTOR('',#11691,1.);
#3182=VECTOR('',#11692,1.);
#3183=VECTOR('',#11695,1.);
#3184=VECTOR('',#11696,1.);
#3185=VECTOR('',#11697,1.);
#3186=VECTOR('',#11700,1.);
#3187=VECTOR('',#11701,1.);
#3188=VECTOR('',#11718,0.4);
#3189=VECTOR('',#11723,0.425);
#3190=VECTOR('',#11728,0.41);
#3191=VECTOR('',#11737,0.26);
#3192=VECTOR('',#11740,0.25);
#3617=CIRCLE('',#9292,0.24505);
#3618=CIRCLE('',#9294,0.375);
#3619=CIRCLE('',#9296,0.425);
#3620=CIRCLE('',#9298,0.425);
#3621=CIRCLE('',#9300,0.395);
#3622=CIRCLE('',#9302,0.27);
#3623=CIRCLE('',#9304,0.24505);
#4250=VERTEX_POINT('',#14574);
#4251=VERTEX_POINT('',#14575);
#4252=VERTEX_POINT('',#14577);
#4253=VERTEX_POINT('',#14579);
#4254=VERTEX_POINT('',#14583);
#4255=VERTEX_POINT('',#14585);
#4256=VERTEX_POINT('',#14589);
#4257=VERTEX_POINT('',#14591);
#4258=VERTEX_POINT('',#14595);
#4259=VERTEX_POINT('',#14597);
#4260=VERTEX_POINT('',#14601);
#4261=VERTEX_POINT('',#14603);
#4262=VERTEX_POINT('',#14612);
#4263=VERTEX_POINT('',#14615);
#4264=VERTEX_POINT('',#14618);
#4265=VERTEX_POINT('',#14622);
#4266=VERTEX_POINT('',#14626);
#4267=VERTEX_POINT('',#14630);
#4268=VERTEX_POINT('',#14633);
#5202=EDGE_CURVE('',#4250,#4251,#2647,.T.);
#5203=EDGE_CURVE('',#4251,#4252,#2648,.T.);
#5204=EDGE_CURVE('',#4252,#4253,#2649,.T.);
#5205=EDGE_CURVE('',#4250,#4253,#2650,.T.);
#5206=EDGE_CURVE('',#4251,#4254,#2651,.T.);
#5207=EDGE_CURVE('',#4254,#4255,#2652,.T.);
#5208=EDGE_CURVE('',#4255,#4252,#2653,.T.);
#5209=EDGE_CURVE('',#4254,#4256,#2654,.T.);
#5210=EDGE_CURVE('',#4256,#4257,#2655,.T.);
#5211=EDGE_CURVE('',#4257,#4255,#2656,.T.);
#5212=EDGE_CURVE('',#4256,#4258,#2657,.T.);
#5213=EDGE_CURVE('',#4258,#4259,#2658,.T.);
#5214=EDGE_CURVE('',#4259,#4257,#2659,.T.);
#5215=EDGE_CURVE('',#4258,#4260,#2660,.T.);
#5216=EDGE_CURVE('',#4260,#4261,#2661,.T.);
#5217=EDGE_CURVE('',#4261,#4259,#2662,.T.);
#5218=EDGE_CURVE('',#4260,#4250,#2663,.T.);
#5219=EDGE_CURVE('',#4253,#4261,#2664,.T.);
#5220=EDGE_CURVE('',#4262,#4262,#3617,.T.);
#5221=EDGE_CURVE('',#4263,#4263,#3618,.T.);
#5222=EDGE_CURVE('',#4264,#4264,#3619,.T.);
#5223=EDGE_CURVE('',#4264,#4263,#2665,.T.);
#5224=EDGE_CURVE('',#4265,#4265,#3620,.T.);
#5225=EDGE_CURVE('',#4265,#4264,#2666,.T.);
#5226=EDGE_CURVE('',#4266,#4266,#3621,.T.);
#5227=EDGE_CURVE('',#4266,#4265,#2667,.T.);
#5228=EDGE_CURVE('',#4267,#4267,#3622,.T.);
#5229=EDGE_CURVE('',#4268,#4268,#3623,.F.);
#5230=EDGE_CURVE('',#4268,#4267,#2668,.T.);
#5231=EDGE_CURVE('',#4262,#4268,#2669,.T.);
#7090=ORIENTED_EDGE('',*,*,#5202,.T.);
#7091=ORIENTED_EDGE('',*,*,#5203,.T.);
#7092=ORIENTED_EDGE('',*,*,#5204,.T.);
#7093=ORIENTED_EDGE('',*,*,#5205,.F.);
#7094=ORIENTED_EDGE('',*,*,#5206,.T.);
#7095=ORIENTED_EDGE('',*,*,#5207,.T.);
#7096=ORIENTED_EDGE('',*,*,#5208,.T.);
#7097=ORIENTED_EDGE('',*,*,#5203,.F.);
#7098=ORIENTED_EDGE('',*,*,#5209,.T.);
#7099=ORIENTED_EDGE('',*,*,#5210,.T.);
#7100=ORIENTED_EDGE('',*,*,#5211,.T.);
#7101=ORIENTED_EDGE('',*,*,#5207,.F.);
#7102=ORIENTED_EDGE('',*,*,#5212,.T.);
#7103=ORIENTED_EDGE('',*,*,#5213,.T.);
#7104=ORIENTED_EDGE('',*,*,#5214,.T.);
#7105=ORIENTED_EDGE('',*,*,#5210,.F.);
#7106=ORIENTED_EDGE('',*,*,#5215,.T.);
#7107=ORIENTED_EDGE('',*,*,#5216,.T.);
#7108=ORIENTED_EDGE('',*,*,#5217,.T.);
#7109=ORIENTED_EDGE('',*,*,#5213,.F.);
#7110=ORIENTED_EDGE('',*,*,#5218,.T.);
#7111=ORIENTED_EDGE('',*,*,#5205,.T.);
#7112=ORIENTED_EDGE('',*,*,#5219,.T.);
#7113=ORIENTED_EDGE('',*,*,#5216,.F.);
#7114=ORIENTED_EDGE('',*,*,#5218,.F.);
#7115=ORIENTED_EDGE('',*,*,#5215,.F.);
#7116=ORIENTED_EDGE('',*,*,#5212,.F.);
#7117=ORIENTED_EDGE('',*,*,#5209,.F.);
#7118=ORIENTED_EDGE('',*,*,#5206,.F.);
#7119=ORIENTED_EDGE('',*,*,#5202,.F.);
#7120=ORIENTED_EDGE('',*,*,#5219,.F.);
#7121=ORIENTED_EDGE('',*,*,#5204,.F.);
#7122=ORIENTED_EDGE('',*,*,#5208,.F.);
#7123=ORIENTED_EDGE('',*,*,#5211,.F.);
#7124=ORIENTED_EDGE('',*,*,#5214,.F.);
#7125=ORIENTED_EDGE('',*,*,#5217,.F.);
#7126=ORIENTED_EDGE('',*,*,#5220,.F.);
#7127=ORIENTED_EDGE('',*,*,#5221,.F.);
#7128=ORIENTED_EDGE('',*,*,#5222,.F.);
#7129=ORIENTED_EDGE('',*,*,#5223,.T.);
#7130=ORIENTED_EDGE('',*,*,#5221,.T.);
#7131=ORIENTED_EDGE('',*,*,#5223,.F.);
#7132=ORIENTED_EDGE('',*,*,#5224,.F.);
#7133=ORIENTED_EDGE('',*,*,#5225,.T.);
#7134=ORIENTED_EDGE('',*,*,#5222,.T.);
#7135=ORIENTED_EDGE('',*,*,#5225,.F.);
#7136=ORIENTED_EDGE('',*,*,#5226,.F.);
#7137=ORIENTED_EDGE('',*,*,#5227,.T.);
#7138=ORIENTED_EDGE('',*,*,#5224,.T.);
#7139=ORIENTED_EDGE('',*,*,#5227,.F.);
#7140=ORIENTED_EDGE('',*,*,#5226,.T.);
#7141=ORIENTED_EDGE('',*,*,#5228,.F.);
#7142=ORIENTED_EDGE('',*,*,#5229,.F.);
#7143=ORIENTED_EDGE('',*,*,#5230,.T.);
#7144=ORIENTED_EDGE('',*,*,#5228,.T.);
#7145=ORIENTED_EDGE('',*,*,#5230,.F.);
#7146=ORIENTED_EDGE('',*,*,#5220,.T.);
#7147=ORIENTED_EDGE('',*,*,#5231,.T.);
#7148=ORIENTED_EDGE('',*,*,#5229,.T.);
#7149=ORIENTED_EDGE('',*,*,#5231,.F.);
#7374=CYLINDRICAL_SURFACE('',#9297,0.425);
#7375=CYLINDRICAL_SURFACE('',#9305,0.24505);
#7812=ADVANCED_FACE('',(#1481),#1025,.F.);
#7813=ADVANCED_FACE('',(#1482),#1026,.F.);
#7814=ADVANCED_FACE('',(#1483),#1027,.F.);
#7815=ADVANCED_FACE('',(#1484),#1028,.F.);
#7816=ADVANCED_FACE('',(#1485),#1029,.F.);
#7817=ADVANCED_FACE('',(#1486),#1030,.F.);
#7818=ADVANCED_FACE('',(#1487),#1031,.F.);
#7819=ADVANCED_FACE('',(#1488),#1032,.F.);
#7820=ADVANCED_FACE('',(#1489),#1033,.F.);
#7821=ADVANCED_FACE('',(#1490),#1034,.T.);
#7822=ADVANCED_FACE('',(#1491),#358,.T.);
#7823=ADVANCED_FACE('',(#1492),#7374,.T.);
#7824=ADVANCED_FACE('',(#1493),#359,.T.);
#7825=ADVANCED_FACE('',(#1494,#780),#1035,.T.);
#7826=ADVANCED_FACE('',(#1495),#360,.T.);
#7827=ADVANCED_FACE('',(#1496),#7375,.T.);
#7895=CLOSED_SHELL('',(#7812,#7813,#7814,#7815,#7816,#7817,#7818,#7819));
#7896=CLOSED_SHELL('',(#7820,#7821,#7822,#7823,#7824,#7825,#7826,#7827));
#9282=AXIS2_PLACEMENT_3D('',#14572,#11670,#11671);
#9283=AXIS2_PLACEMENT_3D('',#14573,#11672,#11673);
#9284=AXIS2_PLACEMENT_3D('',#14582,#11678,#11679);
#9285=AXIS2_PLACEMENT_3D('',#14588,#11683,#11684);
#9286=AXIS2_PLACEMENT_3D('',#14594,#11688,#11689);
#9287=AXIS2_PLACEMENT_3D('',#14600,#11693,#11694);
#9288=AXIS2_PLACEMENT_3D('',#14606,#11698,#11699);
#9289=AXIS2_PLACEMENT_3D('',#14609,#11702,#11703);
#9290=AXIS2_PLACEMENT_3D('',#14610,#11704,#11705);
#9291=AXIS2_PLACEMENT_3D('',#14611,#11706,#11707);
#9292=AXIS2_PLACEMENT_3D('',#14613,#11708,#11709);
#9293=AXIS2_PLACEMENT_3D('',#14614,#11710,#11711);
#9294=AXIS2_PLACEMENT_3D('',#14616,#11712,#11713);
#9295=AXIS2_PLACEMENT_3D('',#14617,#11714,#11715);
#9296=AXIS2_PLACEMENT_3D('',#14619,#11716,#11717);
#9297=AXIS2_PLACEMENT_3D('',#14621,#11719,#11720);
#9298=AXIS2_PLACEMENT_3D('',#14623,#11721,#11722);
#9299=AXIS2_PLACEMENT_3D('',#14625,#11724,#11725);
#9300=AXIS2_PLACEMENT_3D('',#14627,#11726,#11727);
#9301=AXIS2_PLACEMENT_3D('',#14629,#11729,#11730);
#9302=AXIS2_PLACEMENT_3D('',#14631,#11731,#11732);
#9303=AXIS2_PLACEMENT_3D('',#14632,#11733,#11734);
#9304=AXIS2_PLACEMENT_3D('',#14634,#11735,#11736);
#9305=AXIS2_PLACEMENT_3D('',#14636,#11738,#11739);
#11670=DIRECTION('axis',(0.,0.,1.));
#11671=DIRECTION('refdir',(1.,0.,0.));
#11672=DIRECTION('center_axis',(0.866025403784439,0.,-0.5));
#11673=DIRECTION('ref_axis',(0.5,0.,0.866025403784439));
#11674=DIRECTION('',(-0.5,0.,-0.866025403784439));
#11675=DIRECTION('',(0.,-1.,0.));
#11676=DIRECTION('',(0.5,0.,0.866025403784439));
#11677=DIRECTION('',(0.,-1.,0.));
#11678=DIRECTION('center_axis',(1.20185167898973E-16,0.,-1.));
#11679=DIRECTION('ref_axis',(1.,0.,1.20185167898973E-16));
#11680=DIRECTION('',(-1.,0.,-1.20185167898973E-16));
#11681=DIRECTION('',(0.,-1.,0.));
#11682=DIRECTION('',(1.,0.,1.20185167898973E-16));
#11683=DIRECTION('center_axis',(-0.866025403784439,0.,-0.5));
#11684=DIRECTION('ref_axis',(0.5,0.,-0.866025403784439));
#11685=DIRECTION('',(-0.5,0.,0.866025403784439));
#11686=DIRECTION('',(0.,-1.,0.));
#11687=DIRECTION('',(0.5,0.,-0.866025403784439));
#11688=DIRECTION('center_axis',(-0.866025403784439,0.,0.5));
#11689=DIRECTION('ref_axis',(-0.5,0.,-0.866025403784439));
#11690=DIRECTION('',(0.5,0.,0.866025403784439));
#11691=DIRECTION('',(0.,-1.,0.));
#11692=DIRECTION('',(-0.5,0.,-0.866025403784439));
#11693=DIRECTION('center_axis',(-2.40370335797945E-16,0.,1.));
#11694=DIRECTION('ref_axis',(-1.,0.,-2.40370335797945E-16));
#11695=DIRECTION('',(1.,0.,2.40370335797945E-16));
#11696=DIRECTION('',(0.,-1.,0.));
#11697=DIRECTION('',(-1.,0.,-2.40370335797945E-16));
#11698=DIRECTION('center_axis',(0.866025403784439,0.,0.5));
#11699=DIRECTION('ref_axis',(-0.5,0.,0.866025403784439));
#11700=DIRECTION('',(0.5,0.,-0.866025403784439));
#11701=DIRECTION('',(-0.5,0.,0.866025403784439));
#11702=DIRECTION('center_axis',(0.,1.,0.));
#11703=DIRECTION('ref_axis',(1.,0.,0.));
#11704=DIRECTION('center_axis',(0.,-1.,0.));
#11705=DIRECTION('ref_axis',(0.,0.,-1.));
#11706=DIRECTION('center_axis',(0.,1.,0.));
#11707=DIRECTION('ref_axis',(1.,0.,0.));
#11708=DIRECTION('center_axis',(0.,1.,0.));
#11709=DIRECTION('ref_axis',(1.,0.,0.));
#11710=DIRECTION('center_axis',(0.,1.,0.));
#11711=DIRECTION('ref_axis',(0.,0.,1.));
#11712=DIRECTION('center_axis',(0.,-1.,0.));
#11713=DIRECTION('ref_axis',(1.,0.,0.));
#11714=DIRECTION('center_axis',(0.,-1.,0.));
#11715=DIRECTION('ref_axis',(1.,0.,0.));
#11716=DIRECTION('center_axis',(0.,-1.,0.));
#11717=DIRECTION('ref_axis',(1.,0.,0.));
#11718=DIRECTION('',(0.707106781186548,0.707106781186547,8.65956056235493E-17));
#11719=DIRECTION('center_axis',(0.,-1.,0.));
#11720=DIRECTION('ref_axis',(1.,0.,0.));
#11721=DIRECTION('center_axis',(0.,-1.,0.));
#11722=DIRECTION('ref_axis',(1.,0.,0.));
#11723=DIRECTION('',(0.,1.,0.));
#11724=DIRECTION('center_axis',(0.,1.,0.));
#11725=DIRECTION('ref_axis',(1.,0.,0.));
#11726=DIRECTION('center_axis',(0.,-1.,0.));
#11727=DIRECTION('ref_axis',(1.,0.,0.));
#11728=DIRECTION('',(-0.707106781186547,0.707106781186548,-8.65956056235493E-17));
#11729=DIRECTION('center_axis',(0.,-1.,0.));
#11730=DIRECTION('ref_axis',(0.,0.,-1.));
#11731=DIRECTION('center_axis',(0.,-1.,0.));
#11732=DIRECTION('ref_axis',(1.,0.,0.));
#11733=DIRECTION('center_axis',(0.,1.,0.));
#11734=DIRECTION('ref_axis',(1.,0.,0.));
#11735=DIRECTION('center_axis',(0.,1.,0.));
#11736=DIRECTION('ref_axis',(1.,0.,0.));
#11737=DIRECTION('',(-0.447213595499958,0.894427190999916,-5.47678698264203E-17));
#11738=DIRECTION('center_axis',(0.,-1.,0.));
#11739=DIRECTION('ref_axis',(1.,0.,0.));
#11740=DIRECTION('',(0.,1.,0.));
#14572=CARTESIAN_POINT('',(0.,0.,0.));
#14573=CARTESIAN_POINT('Origin',(0.115470053837925,-0.5,-0.2));
#14574=CARTESIAN_POINT('',(0.23094010767585,-0.5,0.));
#14575=CARTESIAN_POINT('',(0.115470053837925,-0.5,-0.2));
#14576=CARTESIAN_POINT('',(0.23094010767585,-0.5,0.));
#14577=CARTESIAN_POINT('',(0.115470053837925,-0.8,-0.2));
#14578=CARTESIAN_POINT('',(0.115470053837925,-0.5,-0.2));
#14579=CARTESIAN_POINT('',(0.23094010767585,-0.8,0.));
#14580=CARTESIAN_POINT('',(0.23094010767585,-0.8,0.));
#14581=CARTESIAN_POINT('',(0.23094010767585,-0.5,0.));
#14582=CARTESIAN_POINT('Origin',(-0.115470053837925,-0.5,-0.2));
#14583=CARTESIAN_POINT('',(-0.115470053837925,-0.5,-0.2));
#14584=CARTESIAN_POINT('',(0.115470053837925,-0.5,-0.2));
#14585=CARTESIAN_POINT('',(-0.115470053837925,-0.8,-0.2));
#14586=CARTESIAN_POINT('',(-0.115470053837925,-0.5,-0.2));
#14587=CARTESIAN_POINT('',(0.115470053837925,-0.8,-0.2));
#14588=CARTESIAN_POINT('Origin',(-0.23094010767585,-0.5,-2.77555756156289E-17));
#14589=CARTESIAN_POINT('',(-0.23094010767585,-0.5,-2.82820063659975E-17));
#14590=CARTESIAN_POINT('',(-0.115470053837925,-0.5,-0.2));
#14591=CARTESIAN_POINT('',(-0.23094010767585,-0.8,-2.77555756156289E-17));
#14592=CARTESIAN_POINT('',(-0.23094010767585,-0.5,-2.82820063659975E-17));
#14593=CARTESIAN_POINT('',(-0.115470053837925,-0.8,-0.2));
#14594=CARTESIAN_POINT('Origin',(-0.115470053837925,-0.5,0.2));
#14595=CARTESIAN_POINT('',(-0.115470053837925,-0.5,0.2));
#14596=CARTESIAN_POINT('',(-0.23094010767585,-0.5,-2.82820063659975E-17));
#14597=CARTESIAN_POINT('',(-0.115470053837925,-0.8,0.2));
#14598=CARTESIAN_POINT('',(-0.115470053837925,-0.5,0.2));
#14599=CARTESIAN_POINT('',(-0.23094010767585,-0.8,-2.82820063659975E-17));
#14600=CARTESIAN_POINT('Origin',(0.115470053837925,-0.5,0.2));
#14601=CARTESIAN_POINT('',(0.115470053837925,-0.5,0.2));
#14602=CARTESIAN_POINT('',(-0.115470053837925,-0.5,0.2));
#14603=CARTESIAN_POINT('',(0.115470053837925,-0.8,0.2));
#14604=CARTESIAN_POINT('',(0.115470053837925,-0.5,0.2));
#14605=CARTESIAN_POINT('',(-0.115470053837925,-0.8,0.2));
#14606=CARTESIAN_POINT('Origin',(0.23094010767585,-0.5,0.));
#14607=CARTESIAN_POINT('',(0.115470053837925,-0.5,0.2));
#14608=CARTESIAN_POINT('',(0.115470053837925,-0.8,0.2));
#14609=CARTESIAN_POINT('Origin',(0.,-0.5,0.));
#14610=CARTESIAN_POINT('Origin',(0.,-0.8,0.));
#14611=CARTESIAN_POINT('Origin',(0.,-1.4,0.));
#14612=CARTESIAN_POINT('',(-0.24505,-1.4,3.00099698131059E-17));
#14613=CARTESIAN_POINT('Origin',(0.,-1.4,0.));
#14614=CARTESIAN_POINT('Origin',(0.375,0.5,0.));
#14615=CARTESIAN_POINT('',(-0.375,0.5,-4.59242549680257E-17));
#14616=CARTESIAN_POINT('Origin',(0.,0.5,0.));
#14617=CARTESIAN_POINT('Origin',(0.,0.475,0.));
#14618=CARTESIAN_POINT('',(-0.425,0.45,-5.20474889637625E-17));
#14619=CARTESIAN_POINT('Origin',(0.,0.45,0.));
#14620=CARTESIAN_POINT('',(-0.4,0.475,-4.89858719658941E-17));
#14621=CARTESIAN_POINT('Origin',(0.,0.24,0.));
#14622=CARTESIAN_POINT('',(-0.425,0.0299999999999998,-5.20474889637625E-17));
#14623=CARTESIAN_POINT('Origin',(0.,0.0299999999999998,0.));
#14624=CARTESIAN_POINT('',(-0.425,0.24,-5.20474889637625E-17));
#14625=CARTESIAN_POINT('Origin',(0.,0.0150000000000001,0.));
#14626=CARTESIAN_POINT('',(-0.395,4.85722573273506E-17,-4.83735485663204E-17));
#14627=CARTESIAN_POINT('Origin',(0.,0.,0.));
#14628=CARTESIAN_POINT('',(-0.41,0.0150000000000001,-5.02105187650415E-17));
#14629=CARTESIAN_POINT('Origin',(0.27,0.,0.));
#14630=CARTESIAN_POINT('',(-0.27,0.,-3.30654635769785E-17));
#14631=CARTESIAN_POINT('Origin',(0.,0.,0.));
#14632=CARTESIAN_POINT('Origin',(0.,-0.02,0.));
#14633=CARTESIAN_POINT('',(-0.24505,-0.0498999999999999,3.00099698131059E-17));
#14634=CARTESIAN_POINT('Origin',(0.,-0.0498999999999999,0.));
#14635=CARTESIAN_POINT('',(-0.26,-0.02,-3.18408167778312E-17));
#14636=CARTESIAN_POINT('Origin',(0.,-0.995,0.));
#14637=CARTESIAN_POINT('',(-0.24505,-0.995,-3.00099698131059E-17));
#14822=UNCERTAINTY_MEASURE_WITH_UNIT(LENGTH_MEASURE(0.001),#14879,
'DISTANCE_ACCURACY_VALUE',
'Maximum model space distance between geometric entities at asserted c
onnectivities');
#14824=UNCERTAINTY_MEASURE_WITH_UNIT(LENGTH_MEASURE(0.001),#14879,
'DISTANCE_ACCURACY_VALUE',
'Maximum model space distance between geometric entities at asserted c
onnectivities');
#14876=(
GEOMETRIC_REPRESENTATION_CONTEXT(3)
GLOBAL_UNCERTAINTY_ASSIGNED_CONTEXT((#14822))
GLOBAL_UNIT_ASSIGNED_CONTEXT((#14879,#14881,#14882))
REPRESENTATION_CONTEXT('','3D')
);
#14878=(
GEOMETRIC_REPRESENTATION_CONTEXT(3)
GLOBAL_UNCERTAINTY_ASSIGNED_CONTEXT((#14824))
GLOBAL_UNIT_ASSIGNED_CONTEXT((#14879,#14881,#14882))
REPRESENTATION_CONTEXT('','3D')
);
#14879=(
LENGTH_UNIT()
NAMED_UNIT(*)
SI_UNIT(.CENTI.,.METRE.)
);
#14881=(
NAMED_UNIT(*)
PLANE_ANGLE_UNIT()
SI_UNIT($,.RADIAN.)
);
#14882=(
NAMED_UNIT(*)
SI_UNIT($,.STERADIAN.)
SOLID_ANGLE_UNIT()
);
#14934=SHAPE_DEFINITION_REPRESENTATION(#14999,#15119);
#14999=PRODUCT_DEFINITION_SHAPE('',$,#15173);
#15119=SHAPE_REPRESENTATION('',(#9282),#14876);
#15121=PRODUCT_DEFINITION_CONTEXT('part definition',#15282,'design');
#15173=PRODUCT_DEFINITION('M5x14 Cap Screw','M5x14 Cap Screw',#15226,#15121);
#15226=PRODUCT_DEFINITION_FORMATION('',$,#15335);
#15282=APPLICATION_CONTEXT(
'Core Data for Automotive Mechanical Design Process');
#15283=PRODUCT_CONTEXT('part definition',#15282,'mechanical');
#15335=PRODUCT('M5x14 Cap Screw','M5x14 Cap Screw','M5x14 Cap Screw',(#15283));
#15407=COLOUR_RGB('Black',0.12,0.14,0.17);
#15408=FILL_AREA_STYLE_COLOUR('',#15407);
#15409=FILL_AREA_STYLE('',(#15408));
#15410=SURFACE_STYLE_FILL_AREA(#15409);
#15411=SURFACE_SIDE_STYLE('',(#15410));
#15412=SURFACE_STYLE_USAGE(.BOTH.,#15411);
#15413=PRESENTATION_STYLE_ASSIGNMENT((#15412));
ENDSEC;
END-ISO-10303-21;
